ISO-10303-21;
HEADER;
/* Generated by software containing ST-Developer
 * from STEP Tools, Inc. (www.steptools.com) 
 */

FILE_DESCRIPTION(
/* description */ ('Vibration shaker table dummy'),
/* implementation_level */ '2;1');

FILE_NAME(
/* name */ 'Cap Screw - M5x20.step',
/* time_stamp */ '2026-10-27T10:55:14-07:00',
/* author */ (''),
/* organization */ (''),
/* preprocessor_version */ 'ST-DEVELOPER v20.2',
/* originating_system */ 'Autodesk Translation Framework v15.17.0.0',
/* authorisation */ '');

FILE_SCHEMA (('AUTOMOTIVE_DESIGN { 1 0 10303 214 3 1 1 }'));
ENDSEC;

DATA;
#10=MECHANICAL_DESIGN_GEOMETRIC_PRESENTATION_REPRESENTATION('',(#722),#22394);
#568=ORIENTED_CLOSED_SHELL('',*,#9242,.F.);
#571=BREP_WITH_VOIDS('Body1',#9241,(#568));
#578=CONICAL_SURFACE('',#10414,0.4,0.785398163397448);
#579=CONICAL_SURFACE('',#10418,0.41,0.785398163397448);
#580=CONICAL_SURFACE('',#10422,0.26,0.463647609000806);
#581=CONICAL_SURFACE('',#10426,0.225,0.785398163397448);
#630=SHAPE_REPRESENTATION_RELATIONSHIP('SRR','None',#22676,#676);
#676=ADVANCED_BREP_SHAPE_REPRESENTATION('',(#571),#22382);
#722=STYLED_ITEM('',(#22968),#571);
#958=FACE_BOUND('',#2363,.T.);
#1261=PLANE('',#10412);
#1262=PLANE('',#10420);
#1263=PLANE('',#10428);
#1264=PLANE('',#10429);
#1265=PLANE('',#10430);
#1266=PLANE('',#10431);
#1267=PLANE('',#10432);
#1268=PLANE('',#10433);
#1269=PLANE('',#10434);
#1270=PLANE('',#10435);
#1271=PLANE('',#10436);
#1677=FACE_OUTER_BOUND('',#2358,.T.);
#1678=FACE_OUTER_BOUND('',#2359,.T.);
#1679=FACE_OUTER_BOUND('',#2360,.T.);
#1680=FACE_OUTER_BOUND('',#2361,.T.);
#1681=FACE_OUTER_BOUND('',#2362,.T.);
#1682=FACE_OUTER_BOUND('',#2364,.T.);
#1683=FACE_OUTER_BOUND('',#2365,.T.);
#1684=FACE_OUTER_BOUND('',#2366,.T.);
#1685=FACE_OUTER_BOUND('',#2367,.T.);
#1686=FACE_OUTER_BOUND('',#2368,.T.);
#1687=FACE_OUTER_BOUND('',#2369,.T.);
#1688=FACE_OUTER_BOUND('',#2370,.T.);
#1689=FACE_OUTER_BOUND('',#2371,.T.);
#1690=FACE_OUTER_BOUND('',#2372,.T.);
#1691=FACE_OUTER_BOUND('',#2373,.T.);
#1692=FACE_OUTER_BOUND('',#2374,.T.);
#1693=FACE_OUTER_BOUND('',#2375,.T.);
#2358=EDGE_LOOP('',(#7694));
#2359=EDGE_LOOP('',(#7695,#7696,#7697,#7698));
#2360=EDGE_LOOP('',(#7699,#7700,#7701,#7702));
#2361=EDGE_LOOP('',(#7703,#7704,#7705,#7706));
#2362=EDGE_LOOP('',(#7707));
#2363=EDGE_LOOP('',(#7708));
#2364=EDGE_LOOP('',(#7709,#7710,#7711,#7712));
#2365=EDGE_LOOP('',(#7713,#7714,#7715,#7716));
#2366=EDGE_LOOP('',(#7717,#7718,#7719,#7720));
#2367=EDGE_LOOP('',(#7721));
#2368=EDGE_LOOP('',(#7722,#7723,#7724,#7725));
#2369=EDGE_LOOP('',(#7726,#7727,#7728,#7729));
#2370=EDGE_LOOP('',(#7730,#7731,#7732,#7733));
#2371=EDGE_LOOP('',(#7734,#7735,#7736,#7737));
#2372=EDGE_LOOP('',(#7738,#7739,#7740,#7741));
#2373=EDGE_LOOP('',(#7742,#7743,#7744,#7745));
#2374=EDGE_LOOP('',(#7746,#7747,#7748,#7749,#7750,#7751));
#2375=EDGE_LOOP('',(#7752,#7753,#7754,#7755,#7756,#7757));
#3061=LINE('',#21313,#3680);
#3062=LINE('',#21317,#3681);
#3063=LINE('',#21321,#3682);
#3064=LINE('',#21328,#3683);
#3065=LINE('',#21332,#3684);
#3066=LINE('',#21336,#3685);
#3067=LINE('',#21341,#3686);
#3068=LINE('',#21343,#3687);
#3069=LINE('',#21345,#3688);
#3070=LINE('',#21346,#3689);
#3071=LINE('',#21349,#3690);
#3072=LINE('',#21351,#3691);
#3073=LINE('',#21352,#3692);
#3074=LINE('',#21355,#3693);
#3075=LINE('',#21357,#3694);
#3076=LINE('',#21358,#3695);
#3077=LINE('',#21361,#3696);
#3078=LINE('',#21363,#3697);
#3079=LINE('',#21364,#3698);
#3080=LINE('',#21367,#3699);
#3081=LINE('',#21369,#3700);
#3082=LINE('',#21370,#3701);
#3083=LINE('',#21372,#3702);
#3084=LINE('',#21373,#3703);
#3680=VECTOR('',#12701,0.4);
#3681=VECTOR('',#12706,0.425);
#3682=VECTOR('',#12711,0.41);
#3683=VECTOR('',#12720,0.26);
#3684=VECTOR('',#12725,0.25);
#3685=VECTOR('',#12730,0.225);
#3686=VECTOR('',#12735,1.);
#3687=VECTOR('',#12736,1.);
#3688=VECTOR('',#12737,1.);
#3689=VECTOR('',#12738,1.);
#3690=VECTOR('',#12741,1.);
#3691=VECTOR('',#12742,1.);
#3692=VECTOR('',#12743,1.);
#3693=VECTOR('',#12746,1.);
#3694=VECTOR('',#12747,1.);
#3695=VECTOR('',#12748,1.);
#3696=VECTOR('',#12751,1.);
#3697=VECTOR('',#12752,1.);
#3698=VECTOR('',#12753,1.);
#3699=VECTOR('',#12756,1.);
#3700=VECTOR('',#12757,1.);
#3701=VECTOR('',#12758,1.);
#3702=VECTOR('',#12761,1.);
#3703=VECTOR('',#12762,1.);
#4141=CIRCLE('',#10413,0.375);
#4142=CIRCLE('',#10415,0.425);
#4143=CIRCLE('',#10417,0.425);
#4144=CIRCLE('',#10419,0.395);
#4145=CIRCLE('',#10421,0.27);
#4146=CIRCLE('',#10423,0.24505);
#4147=CIRCLE('',#10425,0.24505);
#4148=CIRCLE('',#10427,0.2);
#4848=VERTEX_POINT('',#21308);
#4849=VERTEX_POINT('',#21311);
#4850=VERTEX_POINT('',#21315);
#4851=VERTEX_POINT('',#21319);
#4852=VERTEX_POINT('',#21323);
#4853=VERTEX_POINT('',#21326);
#4854=VERTEX_POINT('',#21330);
#4855=VERTEX_POINT('',#21334);
#4856=VERTEX_POINT('',#21339);
#4857=VERTEX_POINT('',#21340);
#4858=VERTEX_POINT('',#21342);
#4859=VERTEX_POINT('',#21344);
#4860=VERTEX_POINT('',#21348);
#4861=VERTEX_POINT('',#21350);
#4862=VERTEX_POINT('',#21354);
#4863=VERTEX_POINT('',#21356);
#4864=VERTEX_POINT('',#21360);
#4865=VERTEX_POINT('',#21362);
#4866=VERTEX_POINT('',#21366);
#4867=VERTEX_POINT('',#21368);
#5840=EDGE_CURVE('',#4848,#4848,#4141,.T.);
#5841=EDGE_CURVE('',#4849,#4849,#4142,.T.);
#5842=EDGE_CURVE('',#4849,#4848,#3061,.T.);
#5843=EDGE_CURVE('',#4850,#4850,#4143,.T.);
#5844=EDGE_CURVE('',#4850,#4849,#3062,.T.);
#5845=EDGE_CURVE('',#4851,#4851,#4144,.T.);
#5846=EDGE_CURVE('',#4851,#4850,#3063,.T.);
#5847=EDGE_CURVE('',#4852,#4852,#4145,.T.);
#5848=EDGE_CURVE('',#4853,#4853,#4146,.F.);
#5849=EDGE_CURVE('',#4853,#4852,#3064,.T.);
#5850=EDGE_CURVE('',#4854,#4854,#4147,.F.);
#5851=EDGE_CURVE('',#4854,#4853,#3065,.T.);
#5852=EDGE_CURVE('',#4855,#4855,#4148,.T.);
#5853=EDGE_CURVE('',#4855,#4854,#3066,.T.);
#5854=EDGE_CURVE('',#4856,#4857,#3067,.T.);
#5855=EDGE_CURVE('',#4857,#4858,#3068,.T.);
#5856=EDGE_CURVE('',#4858,#4859,#3069,.T.);
#5857=EDGE_CURVE('',#4856,#4859,#3070,.T.);
#5858=EDGE_CURVE('',#4857,#4860,#3071,.T.);
#5859=EDGE_CURVE('',#4860,#4861,#3072,.T.);
#5860=EDGE_CURVE('',#4861,#4858,#3073,.T.);
#5861=EDGE_CURVE('',#4860,#4862,#3074,.T.);
#5862=EDGE_CURVE('',#4862,#4863,#3075,.T.);
#5863=EDGE_CURVE('',#4863,#4861,#3076,.T.);
#5864=EDGE_CURVE('',#4862,#4864,#3077,.T.);
#5865=EDGE_CURVE('',#4864,#4865,#3078,.T.);
#5866=EDGE_CURVE('',#4865,#4863,#3079,.T.);
#5867=EDGE_CURVE('',#4864,#4866,#3080,.T.);
#5868=EDGE_CURVE('',#4866,#4867,#3081,.T.);
#5869=EDGE_CURVE('',#4867,#4865,#3082,.T.);
#5870=EDGE_CURVE('',#4866,#4856,#3083,.T.);
#5871=EDGE_CURVE('',#4859,#4867,#3084,.T.);
#7694=ORIENTED_EDGE('',*,*,#5840,.F.);
#7695=ORIENTED_EDGE('',*,*,#5841,.F.);
#7696=ORIENTED_EDGE('',*,*,#5842,.T.);
#7697=ORIENTED_EDGE('',*,*,#5840,.T.);
#7698=ORIENTED_EDGE('',*,*,#5842,.F.);
#7699=ORIENTED_EDGE('',*,*,#5843,.F.);
#7700=ORIENTED_EDGE('',*,*,#5844,.T.);
#7701=ORIENTED_EDGE('',*,*,#5841,.T.);
#7702=ORIENTED_EDGE('',*,*,#5844,.F.);
#7703=ORIENTED_EDGE('',*,*,#5845,.F.);
#7704=ORIENTED_EDGE('',*,*,#5846,.T.);
#7705=ORIENTED_EDGE('',*,*,#5843,.T.);
#7706=ORIENTED_EDGE('',*,*,#5846,.F.);
#7707=ORIENTED_EDGE('',*,*,#5845,.T.);
#7708=ORIENTED_EDGE('',*,*,#5847,.F.);
#7709=ORIENTED_EDGE('',*,*,#5848,.F.);
#7710=ORIENTED_EDGE('',*,*,#5849,.T.);
#7711=ORIENTED_EDGE('',*,*,#5847,.T.);
#7712=ORIENTED_EDGE('',*,*,#5849,.F.);
#7713=ORIENTED_EDGE('',*,*,#5850,.F.);
#7714=ORIENTED_EDGE('',*,*,#5851,.T.);
#7715=ORIENTED_EDGE('',*,*,#5848,.T.);
#7716=ORIENTED_EDGE('',*,*,#5851,.F.);
#7717=ORIENTED_EDGE('',*,*,#5852,.F.);
#7718=ORIENTED_EDGE('',*,*,#5853,.T.);
#7719=ORIENTED_EDGE('',*,*,#5850,.T.);
#7720=ORIENTED_EDGE('',*,*,#5853,.F.);
#7721=ORIENTED_EDGE('',*,*,#5852,.T.);
#7722=ORIENTED_EDGE('',*,*,#5854,.T.);
#7723=ORIENTED_EDGE('',*,*,#5855,.T.);
#7724=ORIENTED_EDGE('',*,*,#5856,.T.);
#7725=ORIENTED_EDGE('',*,*,#5857,.F.);
#7726=ORIENTED_EDGE('',*,*,#5858,.T.);
#7727=ORIENTED_EDGE('',*,*,#5859,.T.);
#7728=ORIENTED_EDGE('',*,*,#5860,.T.);
#7729=ORIENTED_EDGE('',*,*,#5855,.F.);
#7730=ORIENTED_EDGE('',*,*,#5861,.T.);
#7731=ORIENTED_EDGE('',*,*,#5862,.T.);
#7732=ORIENTED_EDGE('',*,*,#5863,.T.);
#7733=ORIENTED_EDGE('',*,*,#5859,.F.);
#7734=ORIENTED_EDGE('',*,*,#5864,.T.);
#7735=ORIENTED_EDGE('',*,*,#5865,.T.);
#7736=ORIENTED_EDGE('',*,*,#5866,.T.);
#7737=ORIENTED_EDGE('',*,*,#5862,.F.);
#7738=ORIENTED_EDGE('',*,*,#5867,.T.);
#7739=ORIENTED_EDGE('',*,*,#5868,.T.);
#7740=ORIENTED_EDGE('',*,*,#5869,.T.);
#7741=ORIENTED_EDGE('',*,*,#5865,.F.);
#7742=ORIENTED_EDGE('',*,*,#5870,.T.);
#7743=ORIENTED_EDGE('',*,*,#5857,.T.);
#7744=ORIENTED_EDGE('',*,*,#5871,.T.);
#7745=ORIENTED_EDGE('',*,*,#5868,.F.);
#7746=ORIENTED_EDGE('',*,*,#5870,.F.);
#7747=ORIENTED_EDGE('',*,*,#5867,.F.);
#7748=ORIENTED_EDGE('',*,*,#5864,.F.);
#7749=ORIENTED_EDGE('',*,*,#5861,.F.);
#7750=ORIENTED_EDGE('',*,*,#5858,.F.);
#7751=ORIENTED_EDGE('',*,*,#5854,.F.);
#7752=ORIENTED_EDGE('',*,*,#5871,.F.);
#7753=ORIENTED_EDGE('',*,*,#5856,.F.);
#7754=ORIENTED_EDGE('',*,*,#5860,.F.);
#7755=ORIENTED_EDGE('',*,*,#5863,.F.);
#7756=ORIENTED_EDGE('',*,*,#5866,.F.);
#7757=ORIENTED_EDGE('',*,*,#5869,.F.);
#8632=CYLINDRICAL_SURFACE('',#10416,0.425);
#8633=CYLINDRICAL_SURFACE('',#10424,0.24505);
#9042=ADVANCED_FACE('',(#1677),#1261,.T.);
#9043=ADVANCED_FACE('',(#1678),#578,.T.);
#9044=ADVANCED_FACE('',(#1679),#8632,.T.);
#9045=ADVANCED_FACE('',(#1680),#579,.T.);
#9046=ADVANCED_FACE('',(#1681,#958),#1262,.T.);
#9047=ADVANCED_FACE('',(#1682),#580,.T.);
#9048=ADVANCED_FACE('',(#1683),#8633,.T.);
#9049=ADVANCED_FACE('',(#1684),#581,.T.);
#9050=ADVANCED_FACE('',(#1685),#1263,.T.);
#9051=ADVANCED_FACE('',(#1686),#1264,.F.);
#9052=ADVANCED_FACE('',(#1687),#1265,.F.);
#9053=ADVANCED_FACE('',(#1688),#1266,.F.);
#9054=ADVANCED_FACE('',(#1689),#1267,.F.);
#9055=ADVANCED_FACE('',(#1690),#1268,.F.);
#9056=ADVANCED_FACE('',(#1691),#1269,.F.);
#9057=ADVANCED_FACE('',(#1692),#1270,.F.);
#9058=ADVANCED_FACE('',(#1693),#1271,.F.);
#9241=CLOSED_SHELL('',(#9042,#9043,#9044,#9045,#9046,#9047,#9048,#9049,
#9050));
#9242=CLOSED_SHELL('',(#9051,#9052,#9053,#9054,#9055,#9056,#9057,#9058));
#10411=AXIS2_PLACEMENT_3D('',#21306,#12691,#12692);
#10412=AXIS2_PLACEMENT_3D('',#21307,#12693,#12694);
#10413=AXIS2_PLACEMENT_3D('',#21309,#12695,#12696);
#10414=AXIS2_PLACEMENT_3D('',#21310,#12697,#12698);
#10415=AXIS2_PLACEMENT_3D('',#21312,#12699,#12700);
#10416=AXIS2_PLACEMENT_3D('',#21314,#12702,#12703);
#10417=AXIS2_PLACEMENT_3D('',#21316,#12704,#12705);
#10418=AXIS2_PLACEMENT_3D('',#21318,#12707,#12708);
#10419=AXIS2_PLACEMENT_3D('',#21320,#12709,#12710);
#10420=AXIS2_PLACEMENT_3D('',#21322,#12712,#12713);
#10421=AXIS2_PLACEMENT_3D('',#21324,#12714,#12715);
#10422=AXIS2_PLACEMENT_3D('',#21325,#12716,#12717);
#10423=AXIS2_PLACEMENT_3D('',#21327,#12718,#12719);
#10424=AXIS2_PLACEMENT_3D('',#21329,#12721,#12722);
#10425=AXIS2_PLACEMENT_3D('',#21331,#12723,#12724);
#10426=AXIS2_PLACEMENT_3D('',#21333,#12726,#12727);
#10427=AXIS2_PLACEMENT_3D('',#21335,#12728,#12729);
#10428=AXIS2_PLACEMENT_3D('',#21337,#12731,#12732);
#10429=AXIS2_PLACEMENT_3D('',#21338,#12733,#12734);
#10430=AXIS2_PLACEMENT_3D('',#21347,#12739,#12740);
#10431=AXIS2_PLACEMENT_3D('',#21353,#12744,#12745);
#10432=AXIS2_PLACEMENT_3D('',#21359,#12749,#12750);
#10433=AXIS2_PLACEMENT_3D('',#21365,#12754,#12755);
#10434=AXIS2_PLACEMENT_3D('',#21371,#12759,#12760);
#10435=AXIS2_PLACEMENT_3D('',#21374,#12763,#12764);
#10436=AXIS2_PLACEMENT_3D('',#21375,#12765,#12766);
#12691=DIRECTION('axis',(0.,0.,1.));
#12692=DIRECTION('refdir',(1.,0.,0.));
#12693=DIRECTION('center_axis',(0.,1.,0.));
#12694=DIRECTION('ref_axis',(0.,0.,1.));
#12695=DIRECTION('center_axis',(0.,-1.,0.));
#12696=DIRECTION('ref_axis',(1.,0.,0.));
#12697=DIRECTION('center_axis',(0.,-1.,0.));
#12698=DIRECTION('ref_axis',(1.,0.,0.));
#12699=DIRECTION('center_axis',(0.,-1.,0.));
#12700=DIRECTION('ref_axis',(1.,0.,0.));
#12701=DIRECTION('',(0.707106781186548,0.707106781186547,8.65956056235493E-17));
#12702=DIRECTION('center_axis',(0.,-1.,0.));
#12703=DIRECTION('ref_axis',(1.,0.,0.));
#12704=DIRECTION('center_axis',(0.,-1.,0.));
#12705=DIRECTION('ref_axis',(1.,0.,0.));
#12706=DIRECTION('',(0.,1.,0.));
#12707=DIRECTION('center_axis',(0.,1.,0.));
#12708=DIRECTION('ref_axis',(1.,0.,0.));
#12709=DIRECTION('center_axis',(0.,-1.,0.));
#12710=DIRECTION('ref_axis',(1.,0.,0.));
#12711=DIRECTION('',(-0.707106781186547,0.707106781186548,-8.65956056235493E-17));
#12712=DIRECTION('center_axis',(0.,-1.,0.));
#12713=DIRECTION('ref_axis',(0.,0.,-1.));
#12714=DIRECTION('center_axis',(0.,-1.,0.));
#12715=DIRECTION('ref_axis',(1.,0.,0.));
#12716=DIRECTION('center_axis',(0.,1.,0.));
#12717=DIRECTION('ref_axis',(1.,0.,0.));
#12718=DIRECTION('center_axis',(0.,1.,0.));
#12719=DIRECTION('ref_axis',(1.,0.,0.));
#12720=DIRECTION('',(-0.447213595499958,0.894427190999916,-5.47678698264203E-17));
#12721=DIRECTION('center_axis',(0.,-1.,0.));
#12722=DIRECTION('ref_axis',(1.,0.,0.));
#12723=DIRECTION('center_axis',(0.,1.,0.));
#12724=DIRECTION('ref_axis',(1.,0.,0.));
#12725=DIRECTION('',(0.,1.,0.));
#12726=DIRECTION('center_axis',(0.,1.,0.));
#12727=DIRECTION('ref_axis',(1.,0.,0.));
#12728=DIRECTION('center_axis',(0.,-1.,0.));
#12729=DIRECTION('ref_axis',(1.,0.,0.));
#12730=DIRECTION('',(-0.707106781186547,0.707106781186548,-8.65956056235493E-17));
#12731=DIRECTION('center_axis',(0.,-1.,0.));
#12732=DIRECTION('ref_axis',(0.,0.,-1.));
#12733=DIRECTION('center_axis',(0.866025403784439,0.,-0.5));
#12734=DIRECTION('ref_axis',(0.5,0.,0.866025403784439));
#12735=DIRECTION('',(-0.5,0.,-0.866025403784439));
#12736=DIRECTION('',(0.,-1.,0.));
#12737=DIRECTION('',(0.5,0.,0.866025403784439));
#12738=DIRECTION('',(0.,-1.,0.));
#12739=DIRECTION('center_axis',(1.20185167898973E-16,0.,-1.));
#12740=DIRECTION('ref_axis',(1.,0.,1.20185167898973E-16));
#12741=DIRECTION('',(-1.,0.,-1.20185167898973E-16));
#12742=DIRECTION('',(0.,-1.,0.));
#12743=DIRECTION('',(1.,0.,1.20185167898973E-16));
#12744=DIRECTION('center_axis',(-0.866025403784439,0.,-0.5));
#12745=DIRECTION('ref_axis',(0.5,0.,-0.866025403784439));
#12746=DIRECTION('',(-0.5,0.,0.866025403784439));
#12747=DIRECTION('',(0.,-1.,0.));
#12748=DIRECTION('',(0.5,0.,-0.866025403784439));
#12749=DIRECTION('center_axis',(-0.866025403784439,0.,0.5));
#12750=DIRECTION('ref_axis',(-0.5,0.,-0.866025403784439));
#12751=DIRECTION('',(0.5,0.,0.866025403784439));
#12752=DIRECTION('',(0.,-1.,0.));
#12753=DIRECTION('',(-0.5,0.,-0.866025403784439));
#12754=DIRECTION('center_axis',(-2.40370335797945E-16,0.,1.));
#12755=DIRECTION('ref_axis',(-1.,0.,-2.40370335797945E-16));
#12756=DIRECTION('',(1.,0.,2.40370335797945E-16));
#12757=DIRECTION('',(0.,-1.,0.));
#12758=DIRECTION('',(-1.,0.,-2.40370335797945E-16));
#12759=DIRECTION('center_axis',(0.866025403784439,0.,0.5));
#12760=DIRECTION('ref_axis',(-0.5,0.,0.866025403784439));
#12761=DIRECTION('',(0.5,0.,-0.866025403784439));
#12762=DIRECTION('',(-0.5,0.,0.866025403784439));
#12763=DIRECTION('center_axis',(0.,1.,0.));
#12764=DIRECTION('ref_axis',(1.,0.,0.));
#12765=DIRECTION('center_axis',(0.,-1.,0.));
#12766=DIRECTION('ref_axis',(0.,0.,-1.));
#21306=CARTESIAN_POINT('',(0.,0.,0.));
#21307=CARTESIAN_POINT('Origin',(0.375,0.5,0.));
#21308=CARTESIAN_POINT('',(-0.375,0.5,-4.59242549680257E-17));
#21309=CARTESIAN_POINT('Origin',(0.,0.5,0.));
#21310=CARTESIAN_POINT('Origin',(0.,0.475,0.));
#21311=CARTESIAN_POINT('',(-0.425,0.45,-5.20474889637625E-17));
#21312=CARTESIAN_POINT('Origin',(0.,0.45,0.));
#21313=CARTESIAN_POINT('',(-0.4,0.475,-4.89858719658941E-17));
#21314=CARTESIAN_POINT('Origin',(0.,0.24,0.));
#21315=CARTESIAN_POINT('',(-0.425,0.0299999999999998,-5.20474889637625E-17));
#21316=CARTESIAN_POINT('Origin',(0.,0.0299999999999998,0.));
#21317=CARTESIAN_POINT('',(-0.425,0.24,-5.20474889637625E-17));
#21318=CARTESIAN_POINT('Origin',(0.,0.0150000000000001,0.));
#21319=CARTESIAN_POINT('',(-0.395,4.85722573273506E-17,-4.83735485663204E-17));
#21320=CARTESIAN_POINT('Origin',(0.,0.,0.));
#21321=CARTESIAN_POINT('',(-0.41,0.0150000000000001,-5.02105187650415E-17));
#21322=CARTESIAN_POINT('Origin',(0.27,0.,0.));
#21323=CARTESIAN_POINT('',(-0.27,0.,-3.30654635769785E-17));
#21324=CARTESIAN_POINT('Origin',(0.,0.,0.));
#21325=CARTESIAN_POINT('Origin',(0.,-0.02,0.));
#21326=CARTESIAN_POINT('',(-0.24505,-0.0498999999999999,3.00099698131059E-17));
#21327=CARTESIAN_POINT('Origin',(0.,-0.0498999999999999,0.));
#21328=CARTESIAN_POINT('',(-0.26,-0.02,-3.18408167778312E-17));
#21329=CARTESIAN_POINT('Origin',(0.,-0.995,0.));
#21330=CARTESIAN_POINT('',(-0.24505,-1.95495,3.00099698131059E-17));
#21331=CARTESIAN_POINT('Origin',(0.,-1.95495,0.));
#21332=CARTESIAN_POINT('',(-0.24505,-0.995,-3.00099698131059E-17));
#21333=CARTESIAN_POINT('Origin',(0.,-1.975,0.));
#21334=CARTESIAN_POINT('',(-0.2,-2.,-2.44929359829471E-17));
#21335=CARTESIAN_POINT('Origin',(0.,-2.,0.));
#21336=CARTESIAN_POINT('',(-0.225,-1.975,-2.75545529808154E-17));
#21337=CARTESIAN_POINT('Origin',(0.,-2.,0.));
#21338=CARTESIAN_POINT('Origin',(0.115470053837925,-0.5,-0.2));
#21339=CARTESIAN_POINT('',(0.23094010767585,-0.5,0.));
#21340=CARTESIAN_POINT('',(0.115470053837925,-0.5,-0.2));
#21341=CARTESIAN_POINT('',(0.23094010767585,-0.5,0.));
#21342=CARTESIAN_POINT('',(0.115470053837925,-0.8,-0.2));
#21343=CARTESIAN_POINT('',(0.115470053837925,-0.5,-0.2));
#21344=CARTESIAN_POINT('',(0.23094010767585,-0.8,0.));
#21345=CARTESIAN_POINT('',(0.23094010767585,-0.8,0.));
#21346=CARTESIAN_POINT('',(0.23094010767585,-0.5,0.));
#21347=CARTESIAN_POINT('Origin',(-0.115470053837925,-0.5,-0.2));
#21348=CARTESIAN_POINT('',(-0.115470053837925,-0.5,-0.2));
#21349=CARTESIAN_POINT('',(0.115470053837925,-0.5,-0.2));
#21350=CARTESIAN_POINT('',(-0.115470053837925,-0.8,-0.2));
#21351=CARTESIAN_POINT('',(-0.115470053837925,-0.5,-0.2));
#21352=CARTESIAN_POINT('',(0.115470053837925,-0.8,-0.2));
#21353=CARTESIAN_POINT('Origin',(-0.23094010767585,-0.5,-2.77555756156289E-17));
#21354=CARTESIAN_POINT('',(-0.23094010767585,-0.5,-2.82820063659975E-17));
#21355=CARTESIAN_POINT('',(-0.115470053837925,-0.5,-0.2));
#21356=CARTESIAN_POINT('',(-0.23094010767585,-0.8,-2.77555756156289E-17));
#21357=CARTESIAN_POINT('',(-0.23094010767585,-0.5,-2.82820063659975E-17));
#21358=CARTESIAN_POINT('',(-0.115470053837925,-0.8,-0.2));
#21359=CARTESIAN_POINT('Origin',(-0.115470053837925,-0.5,0.2));
#21360=CARTESIAN_POINT('',(-0.115470053837925,-0.5,0.2));
#21361=CARTESIAN_POINT('',(-0.23094010767585,-0.5,-2.82820063659975E-17));
#21362=CARTESIAN_POINT('',(-0.115470053837925,-0.8,0.2));
#21363=CARTESIAN_POINT('',(-0.115470053837925,-0.5,0.2));
#21364=CARTESIAN_POINT('',(-0.23094010767585,-0.8,-2.82820063659975E-17));
#21365=CARTESIAN_POINT('Origin',(0.115470053837925,-0.5,0.2));
#21366=CARTESIAN_POINT('',(0.115470053837925,-0.5,0.2));
#21367=CARTESIAN_POINT('',(-0.115470053837925,-0.5,0.2));
#21368=CARTESIAN_POINT('',(0.115470053837925,-0.8,0.2));
#21369=CARTESIAN_POINT('',(0.115470053837925,-0.5,0.2));
#21370=CARTESIAN_POINT('',(-0.115470053837925,-0.8,0.2));
#21371=CARTESIAN_POINT('Origin',(0.23094010767585,-0.5,0.));
#21372=CARTESIAN_POINT('',(0.115470053837925,-0.5,0.2));
#21373=CARTESIAN_POINT('',(0.115470053837925,-0.8,0.2));
#21374=CARTESIAN_POINT('Origin',(0.,-0.5,0.));
#21375=CARTESIAN_POINT('Origin',(0.,-0.8,0.));
#22331=UNCERTAINTY_MEASURE_WITH_UNIT(LENGTH_MEASURE(0.001),#22395,
'DISTANCE_ACCURACY_VALUE',
'Maximum model space distance between geometric entities at asserted c
onnectivities');
#22343=UNCERTAINTY_MEASURE_WITH_UNIT(LENGTH_MEASURE(0.001),#22395,
'DISTANCE_ACCURACY_VALUE',
'Maximum model space distance between geometric entities at asserted c
onnectivities');
#22382=(
GEOMETRIC_REPRESENTATION_CONTEXT(3)
GLOBAL_UNCERTAINTY_ASSIGNED_CONTEXT((#22331))
GLOBAL_UNIT_ASSIGNED_CONTEXT((#22395,#22397,#22398))
REPRESENTATION_CONTEXT('','3D')
);
#22394=(
GEOMETRIC_REPRESENTATION_CONTEXT(3)
GLOBAL_UNCERTAINTY_ASSIGNED_CONTEXT((#22343))
GLOBAL_UNIT_ASSIGNED_CONTEXT((#22395,#22397,#22398))
REPRESENTATION_CONTEXT('','3D')
);
#22395=(
LENGTH_UNIT()
NAMED_UNIT(*)
SI_UNIT(.CENTI.,.METRE.)
);
#22397=(
NAMED_UNIT(*)
PLANE_ANGLE_UNIT()
SI_UNIT($,.RADIAN.)
);
#22398=(
NAMED_UNIT(*)
SI_UNIT($,.STERADIAN.)
SOLID_ANGLE_UNIT()
);
#22437=SHAPE_DEFINITION_REPRESENTATION(#22487,#22676);
#22487=PRODUCT_DEFINITION_SHAPE('',$,#22727);
#22676=SHAPE_REPRESENTATION('',(#10411),#22382);
#22688=PRODUCT_DEFINITION_CONTEXT('part definition',#22840,'design');
#22727=PRODUCT_DEFINITION('Cap Screw - M5x20','Cap Screw - M5x20',#22777,
#22688);
#22777=PRODUCT_DEFINITION_FORMATION('',$,#22880);
#22840=APPLICATION_CONTEXT(
'Core Data for Automotive Mechanical Design Process');
#22841=PRODUCT_CONTEXT('part definition',#22840,'mechanical');
#22880=PRODUCT('Cap Screw - M5x20','Cap Screw - M5x20',
'Cap Screw - M5x20',(#22841));
#22962=COLOUR_RGB('Black',0.12,0.14,0.17);
#22963=FILL_AREA_STYLE_COLOUR('',#22962);
#22964=FILL_AREA_STYLE('',(#22963));
#22965=SURFACE_STYLE_FILL_AREA(#22964);
#22966=SURFACE_SIDE_STYLE('',(#22965));
#22967=SURFACE_STYLE_USAGE(.BOTH.,#22966);
#22968=PRESENTATION_STYLE_ASSIGNMENT((#22967));
ENDSEC;
END-ISO-10303-21;
